ISO-10303-21;
HEADER;
/* Generated by software containing ST-Developer
 * from STEP Tools, Inc. (www.steptools.com) 
 */

FILE_DESCRIPTION(
/* description */ ('PAT-080'),
/* implementation_level */ '2;1');

FILE_NAME(
/* name */ 'Cap Screw - M8x30.step',
/* time_stamp */ '2026-10-29T20:13:47-07:00',
/* author */ (''),
/* organization */ (''),
/* preprocessor_version */ 'ST-DEVELOPER v20.2',
/* originating_system */ 'Autodesk Translation Framework v15.17.0.0',
/* authorisation */ '');

FILE_SCHEMA (('AUTOMOTIVE_DESIGN { 1 0 10303 214 3 1 1 }'));
ENDSEC;

DATA;
#10=MECHANICAL_DESIGN_GEOMETRIC_PRESENTATION_REPRESENTATION('',(#262),#6878);
#196=CONICAL_SURFACE('',#4446,0.625,0.785398163397448);
#197=CONICAL_SURFACE('',#4450,0.635,0.785398163397449);
#198=CONICAL_SURFACE('',#4454,0.41,0.463647609000806);
#199=CONICAL_SURFACE('',#4458,0.36,0.785398163397448);
#204=ORIENTED_CLOSED_SHELL('',*,#3881,.F.);
#207=BREP_WITH_VOIDS('Body1',#3880,(#204));
#224=SHAPE_REPRESENTATION_RELATIONSHIP('SRR','None',#6980,#243);
#243=ADVANCED_BREP_SHAPE_REPRESENTATION('',(#207),#6875);
#262=STYLED_ITEM('',(#7136),#207);
#352=FACE_BOUND('',#996,.T.);
#479=PLANE('',#4444);
#480=PLANE('',#4452);
#481=PLANE('',#4460);
#482=PLANE('',#4461);
#483=PLANE('',#4462);
#484=PLANE('',#4463);
#485=PLANE('',#4464);
#486=PLANE('',#4465);
#487=PLANE('',#4466);
#488=PLANE('',#4467);
#489=PLANE('',#4468);
#694=FACE_OUTER_BOUND('',#991,.T.);
#695=FACE_OUTER_BOUND('',#992,.T.);
#696=FACE_OUTER_BOUND('',#993,.T.);
#697=FACE_OUTER_BOUND('',#994,.T.);
#698=FACE_OUTER_BOUND('',#995,.T.);
#699=FACE_OUTER_BOUND('',#997,.T.);
#700=FACE_OUTER_BOUND('',#998,.T.);
#701=FACE_OUTER_BOUND('',#999,.T.);
#702=FACE_OUTER_BOUND('',#1000,.T.);
#703=FACE_OUTER_BOUND('',#1001,.T.);
#704=FACE_OUTER_BOUND('',#1002,.T.);
#705=FACE_OUTER_BOUND('',#1003,.T.);
#706=FACE_OUTER_BOUND('',#1004,.T.);
#707=FACE_OUTER_BOUND('',#1005,.T.);
#708=FACE_OUTER_BOUND('',#1006,.T.);
#709=FACE_OUTER_BOUND('',#1007,.T.);
#710=FACE_OUTER_BOUND('',#1008,.T.);
#991=EDGE_LOOP('',(#3444));
#992=EDGE_LOOP('',(#3445,#3446,#3447,#3448));
#993=EDGE_LOOP('',(#3449,#3450,#3451,#3452));
#994=EDGE_LOOP('',(#3453,#3454,#3455,#3456));
#995=EDGE_LOOP('',(#3457));
#996=EDGE_LOOP('',(#3458));
#997=EDGE_LOOP('',(#3459,#3460,#3461,#3462));
#998=EDGE_LOOP('',(#3463,#3464,#3465,#3466));
#999=EDGE_LOOP('',(#3467,#3468,#3469,#3470));
#1000=EDGE_LOOP('',(#3471));
#1001=EDGE_LOOP('',(#3472,#3473,#3474,#3475));
#1002=EDGE_LOOP('',(#3476,#3477,#3478,#3479));
#1003=EDGE_LOOP('',(#3480,#3481,#3482,#3483));
#1004=EDGE_LOOP('',(#3484,#3485,#3486,#3487));
#1005=EDGE_LOOP('',(#3488,#3489,#3490,#3491));
#1006=EDGE_LOOP('',(#3492,#3493,#3494,#3495));
#1007=EDGE_LOOP('',(#3496,#3497,#3498,#3499,#3500,#3501));
#1008=EDGE_LOOP('',(#3502,#3503,#3504,#3505,#3506,#3507));
#1308=LINE('',#6642,#1623);
#1309=LINE('',#6646,#1624);
#1310=LINE('',#6650,#1625);
#1311=LINE('',#6657,#1626);
#1312=LINE('',#6661,#1627);
#1313=LINE('',#6665,#1628);
#1314=LINE('',#6670,#1629);
#1315=LINE('',#6672,#1630);
#1316=LINE('',#6674,#1631);
#1317=LINE('',#6675,#1632);
#1318=LINE('',#6678,#1633);
#1319=LINE('',#6680,#1634);
#1320=LINE('',#6681,#1635);
#1321=LINE('',#6684,#1636);
#1322=LINE('',#6686,#1637);
#1323=LINE('',#6687,#1638);
#1324=LINE('',#6690,#1639);
#1325=LINE('',#6692,#1640);
#1326=LINE('',#6693,#1641);
#1327=LINE('',#6696,#1642);
#1328=LINE('',#6698,#1643);
#1329=LINE('',#6699,#1644);
#1330=LINE('',#6701,#1645);
#1331=LINE('',#6702,#1646);
#1623=VECTOR('',#5522,0.625);
#1624=VECTOR('',#5527,0.65);
#1625=VECTOR('',#5532,0.635);
#1626=VECTOR('',#5541,0.41);
#1627=VECTOR('',#5546,0.4);
#1628=VECTOR('',#5551,0.36);
#1629=VECTOR('',#5556,1.);
#1630=VECTOR('',#5557,1.);
#1631=VECTOR('',#5558,1.);
#1632=VECTOR('',#5559,1.);
#1633=VECTOR('',#5562,1.);
#1634=VECTOR('',#5563,1.);
#1635=VECTOR('',#5564,1.);
#1636=VECTOR('',#5567,1.);
#1637=VECTOR('',#5568,1.);
#1638=VECTOR('',#5569,1.);
#1639=VECTOR('',#5572,1.);
#1640=VECTOR('',#5573,1.);
#1641=VECTOR('',#5574,1.);
#1642=VECTOR('',#5577,1.);
#1643=VECTOR('',#5578,1.);
#1644=VECTOR('',#5579,1.);
#1645=VECTOR('',#5582,1.);
#1646=VECTOR('',#5583,1.);
#1794=CIRCLE('',#4445,0.6);
#1795=CIRCLE('',#4447,0.65);
#1796=CIRCLE('',#4449,0.65);
#1797=CIRCLE('',#4451,0.62);
#1798=CIRCLE('',#4453,0.42);
#1799=CIRCLE('',#4455,0.3933);
#1800=CIRCLE('',#4457,0.3933);
#1801=CIRCLE('',#4459,0.32);
#2087=VERTEX_POINT('',#6637);
#2088=VERTEX_POINT('',#6640);
#2089=VERTEX_POINT('',#6644);
#2090=VERTEX_POINT('',#6648);
#2091=VERTEX_POINT('',#6652);
#2092=VERTEX_POINT('',#6655);
#2093=VERTEX_POINT('',#6659);
#2094=VERTEX_POINT('',#6663);
#2095=VERTEX_POINT('',#6668);
#2096=VERTEX_POINT('',#6669);
#2097=VERTEX_POINT('',#6671);
#2098=VERTEX_POINT('',#6673);
#2099=VERTEX_POINT('',#6677);
#2100=VERTEX_POINT('',#6679);
#2101=VERTEX_POINT('',#6683);
#2102=VERTEX_POINT('',#6685);
#2103=VERTEX_POINT('',#6689);
#2104=VERTEX_POINT('',#6691);
#2105=VERTEX_POINT('',#6695);
#2106=VERTEX_POINT('',#6697);
#2545=EDGE_CURVE('',#2087,#2087,#1794,.T.);
#2546=EDGE_CURVE('',#2088,#2088,#1795,.T.);
#2547=EDGE_CURVE('',#2088,#2087,#1308,.T.);
#2548=EDGE_CURVE('',#2089,#2089,#1796,.T.);
#2549=EDGE_CURVE('',#2089,#2088,#1309,.T.);
#2550=EDGE_CURVE('',#2090,#2090,#1797,.T.);
#2551=EDGE_CURVE('',#2090,#2089,#1310,.T.);
#2552=EDGE_CURVE('',#2091,#2091,#1798,.T.);
#2553=EDGE_CURVE('',#2092,#2092,#1799,.F.);
#2554=EDGE_CURVE('',#2092,#2091,#1311,.T.);
#2555=EDGE_CURVE('',#2093,#2093,#1800,.F.);
#2556=EDGE_CURVE('',#2093,#2092,#1312,.T.);
#2557=EDGE_CURVE('',#2094,#2094,#1801,.T.);
#2558=EDGE_CURVE('',#2094,#2093,#1313,.T.);
#2559=EDGE_CURVE('',#2095,#2096,#1314,.T.);
#2560=EDGE_CURVE('',#2096,#2097,#1315,.T.);
#2561=EDGE_CURVE('',#2097,#2098,#1316,.T.);
#2562=EDGE_CURVE('',#2095,#2098,#1317,.T.);
#2563=EDGE_CURVE('',#2096,#2099,#1318,.T.);
#2564=EDGE_CURVE('',#2099,#2100,#1319,.T.);
#2565=EDGE_CURVE('',#2100,#2097,#1320,.T.);
#2566=EDGE_CURVE('',#2099,#2101,#1321,.T.);
#2567=EDGE_CURVE('',#2101,#2102,#1322,.T.);
#2568=EDGE_CURVE('',#2102,#2100,#1323,.T.);
#2569=EDGE_CURVE('',#2101,#2103,#1324,.T.);
#2570=EDGE_CURVE('',#2103,#2104,#1325,.T.);
#2571=EDGE_CURVE('',#2104,#2102,#1326,.T.);
#2572=EDGE_CURVE('',#2103,#2105,#1327,.T.);
#2573=EDGE_CURVE('',#2105,#2106,#1328,.T.);
#2574=EDGE_CURVE('',#2106,#2104,#1329,.T.);
#2575=EDGE_CURVE('',#2105,#2095,#1330,.T.);
#2576=EDGE_CURVE('',#2098,#2106,#1331,.T.);
#3444=ORIENTED_EDGE('',*,*,#2545,.F.);
#3445=ORIENTED_EDGE('',*,*,#2546,.F.);
#3446=ORIENTED_EDGE('',*,*,#2547,.T.);
#3447=ORIENTED_EDGE('',*,*,#2545,.T.);
#3448=ORIENTED_EDGE('',*,*,#2547,.F.);
#3449=ORIENTED_EDGE('',*,*,#2548,.F.);
#3450=ORIENTED_EDGE('',*,*,#2549,.T.);
#3451=ORIENTED_EDGE('',*,*,#2546,.T.);
#3452=ORIENTED_EDGE('',*,*,#2549,.F.);
#3453=ORIENTED_EDGE('',*,*,#2550,.F.);
#3454=ORIENTED_EDGE('',*,*,#2551,.T.);
#3455=ORIENTED_EDGE('',*,*,#2548,.T.);
#3456=ORIENTED_EDGE('',*,*,#2551,.F.);
#3457=ORIENTED_EDGE('',*,*,#2550,.T.);
#3458=ORIENTED_EDGE('',*,*,#2552,.F.);
#3459=ORIENTED_EDGE('',*,*,#2553,.F.);
#3460=ORIENTED_EDGE('',*,*,#2554,.T.);
#3461=ORIENTED_EDGE('',*,*,#2552,.T.);
#3462=ORIENTED_EDGE('',*,*,#2554,.F.);
#3463=ORIENTED_EDGE('',*,*,#2555,.F.);
#3464=ORIENTED_EDGE('',*,*,#2556,.T.);
#3465=ORIENTED_EDGE('',*,*,#2553,.T.);
#3466=ORIENTED_EDGE('',*,*,#2556,.F.);
#3467=ORIENTED_EDGE('',*,*,#2557,.F.);
#3468=ORIENTED_EDGE('',*,*,#2558,.T.);
#3469=ORIENTED_EDGE('',*,*,#2555,.T.);
#3470=ORIENTED_EDGE('',*,*,#2558,.F.);
#3471=ORIENTED_EDGE('',*,*,#2557,.T.);
#3472=ORIENTED_EDGE('',*,*,#2559,.T.);
#3473=ORIENTED_EDGE('',*,*,#2560,.T.);
#3474=ORIENTED_EDGE('',*,*,#2561,.T.);
#3475=ORIENTED_EDGE('',*,*,#2562,.F.);
#3476=ORIENTED_EDGE('',*,*,#2563,.T.);
#3477=ORIENTED_EDGE('',*,*,#2564,.T.);
#3478=ORIENTED_EDGE('',*,*,#2565,.T.);
#3479=ORIENTED_EDGE('',*,*,#2560,.F.);
#3480=ORIENTED_EDGE('',*,*,#2566,.T.);
#3481=ORIENTED_EDGE('',*,*,#2567,.T.);
#3482=ORIENTED_EDGE('',*,*,#2568,.T.);
#3483=ORIENTED_EDGE('',*,*,#2564,.F.);
#3484=ORIENTED_EDGE('',*,*,#2569,.T.);
#3485=ORIENTED_EDGE('',*,*,#2570,.T.);
#3486=ORIENTED_EDGE('',*,*,#2571,.T.);
#3487=ORIENTED_EDGE('',*,*,#2567,.F.);
#3488=ORIENTED_EDGE('',*,*,#2572,.T.);
#3489=ORIENTED_EDGE('',*,*,#2573,.T.);
#3490=ORIENTED_EDGE('',*,*,#2574,.T.);
#3491=ORIENTED_EDGE('',*,*,#2570,.F.);
#3492=ORIENTED_EDGE('',*,*,#2575,.T.);
#3493=ORIENTED_EDGE('',*,*,#2562,.T.);
#3494=ORIENTED_EDGE('',*,*,#2576,.T.);
#3495=ORIENTED_EDGE('',*,*,#2573,.F.);
#3496=ORIENTED_EDGE('',*,*,#2575,.F.);
#3497=ORIENTED_EDGE('',*,*,#2572,.F.);
#3498=ORIENTED_EDGE('',*,*,#2569,.F.);
#3499=ORIENTED_EDGE('',*,*,#2566,.F.);
#3500=ORIENTED_EDGE('',*,*,#2563,.F.);
#3501=ORIENTED_EDGE('',*,*,#2559,.F.);
#3502=ORIENTED_EDGE('',*,*,#2576,.F.);
#3503=ORIENTED_EDGE('',*,*,#2561,.F.);
#3504=ORIENTED_EDGE('',*,*,#2565,.F.);
#3505=ORIENTED_EDGE('',*,*,#2568,.F.);
#3506=ORIENTED_EDGE('',*,*,#2571,.F.);
#3507=ORIENTED_EDGE('',*,*,#2574,.F.);
#3631=CYLINDRICAL_SURFACE('',#4448,0.65);
#3632=CYLINDRICAL_SURFACE('',#4456,0.3933);
#3830=ADVANCED_FACE('',(#694),#479,.T.);
#3831=ADVANCED_FACE('',(#695),#196,.T.);
#3832=ADVANCED_FACE('',(#696),#3631,.T.);
#3833=ADVANCED_FACE('',(#697),#197,.T.);
#3834=ADVANCED_FACE('',(#698,#352),#480,.T.);
#3835=ADVANCED_FACE('',(#699),#198,.T.);
#3836=ADVANCED_FACE('',(#700),#3632,.T.);
#3837=ADVANCED_FACE('',(#701),#199,.T.);
#3838=ADVANCED_FACE('',(#702),#481,.T.);
#3839=ADVANCED_FACE('',(#703),#482,.F.);
#3840=ADVANCED_FACE('',(#704),#483,.F.);
#3841=ADVANCED_FACE('',(#705),#484,.F.);
#3842=ADVANCED_FACE('',(#706),#485,.F.);
#3843=ADVANCED_FACE('',(#707),#486,.F.);
#3844=ADVANCED_FACE('',(#708),#487,.F.);
#3845=ADVANCED_FACE('',(#709),#488,.F.);
#3846=ADVANCED_FACE('',(#710),#489,.F.);
#3880=CLOSED_SHELL('',(#3830,#3831,#3832,#3833,#3834,#3835,#3836,#3837,
#3838));
#3881=CLOSED_SHELL('',(#3839,#3840,#3841,#3842,#3843,#3844,#3845,#3846));
#4443=AXIS2_PLACEMENT_3D('',#6635,#5512,#5513);
#4444=AXIS2_PLACEMENT_3D('',#6636,#5514,#5515);
#4445=AXIS2_PLACEMENT_3D('',#6638,#5516,#5517);
#4446=AXIS2_PLACEMENT_3D('',#6639,#5518,#5519);
#4447=AXIS2_PLACEMENT_3D('',#6641,#5520,#5521);
#4448=AXIS2_PLACEMENT_3D('',#6643,#5523,#5524);
#4449=AXIS2_PLACEMENT_3D('',#6645,#5525,#5526);
#4450=AXIS2_PLACEMENT_3D('',#6647,#5528,#5529);
#4451=AXIS2_PLACEMENT_3D('',#6649,#5530,#5531);
#4452=AXIS2_PLACEMENT_3D('',#6651,#5533,#5534);
#4453=AXIS2_PLACEMENT_3D('',#6653,#5535,#5536);
#4454=AXIS2_PLACEMENT_3D('',#6654,#5537,#5538);
#4455=AXIS2_PLACEMENT_3D('',#6656,#5539,#5540);
#4456=AXIS2_PLACEMENT_3D('',#6658,#5542,#5543);
#4457=AXIS2_PLACEMENT_3D('',#6660,#5544,#5545);
#4458=AXIS2_PLACEMENT_3D('',#6662,#5547,#5548);
#4459=AXIS2_PLACEMENT_3D('',#6664,#5549,#5550);
#4460=AXIS2_PLACEMENT_3D('',#6666,#5552,#5553);
#4461=AXIS2_PLACEMENT_3D('',#6667,#5554,#5555);
#4462=AXIS2_PLACEMENT_3D('',#6676,#5560,#5561);
#4463=AXIS2_PLACEMENT_3D('',#6682,#5565,#5566);
#4464=AXIS2_PLACEMENT_3D('',#6688,#5570,#5571);
#4465=AXIS2_PLACEMENT_3D('',#6694,#5575,#5576);
#4466=AXIS2_PLACEMENT_3D('',#6700,#5580,#5581);
#4467=AXIS2_PLACEMENT_3D('',#6703,#5584,#5585);
#4468=AXIS2_PLACEMENT_3D('',#6704,#5586,#5587);
#5512=DIRECTION('axis',(0.,0.,1.));
#5513=DIRECTION('refdir',(1.,0.,0.));
#5514=DIRECTION('center_axis',(0.,1.,0.));
#5515=DIRECTION('ref_axis',(0.,0.,1.));
#5516=DIRECTION('center_axis',(0.,-1.,0.));
#5517=DIRECTION('ref_axis',(1.,0.,0.));
#5518=DIRECTION('center_axis',(0.,-1.,0.));
#5519=DIRECTION('ref_axis',(1.,0.,0.));
#5520=DIRECTION('center_axis',(0.,-1.,0.));
#5521=DIRECTION('ref_axis',(1.,0.,0.));
#5522=DIRECTION('',(0.707106781186548,0.707106781186547,8.65956056235493E-17));
#5523=DIRECTION('center_axis',(0.,-1.,0.));
#5524=DIRECTION('ref_axis',(1.,0.,0.));
#5525=DIRECTION('center_axis',(0.,-1.,0.));
#5526=DIRECTION('ref_axis',(1.,0.,0.));
#5527=DIRECTION('',(0.,1.,0.));
#5528=DIRECTION('center_axis',(0.,1.,0.));
#5529=DIRECTION('ref_axis',(1.,0.,0.));
#5530=DIRECTION('center_axis',(0.,-1.,0.));
#5531=DIRECTION('ref_axis',(1.,0.,0.));
#5532=DIRECTION('',(-0.707106781186548,0.707106781186547,-8.65956056235494E-17));
#5533=DIRECTION('center_axis',(0.,-1.,0.));
#5534=DIRECTION('ref_axis',(0.,0.,-1.));
#5535=DIRECTION('center_axis',(0.,-1.,0.));
#5536=DIRECTION('ref_axis',(1.,0.,0.));
#5537=DIRECTION('center_axis',(0.,1.,0.));
#5538=DIRECTION('ref_axis',(1.,0.,0.));
#5539=DIRECTION('center_axis',(0.,1.,0.));
#5540=DIRECTION('ref_axis',(1.,0.,0.));
#5541=DIRECTION('',(-0.447213595499958,0.894427190999916,-5.47678698264203E-17));
#5542=DIRECTION('center_axis',(0.,-1.,0.));
#5543=DIRECTION('ref_axis',(1.,0.,0.));
#5544=DIRECTION('center_axis',(0.,1.,0.));
#5545=DIRECTION('ref_axis',(1.,0.,0.));
#5546=DIRECTION('',(0.,1.,0.));
#5547=DIRECTION('center_axis',(0.,1.,0.));
#5548=DIRECTION('ref_axis',(1.,0.,0.));
#5549=DIRECTION('center_axis',(0.,-1.,0.));
#5550=DIRECTION('ref_axis',(1.,0.,0.));
#5551=DIRECTION('',(-0.707106781186547,0.707106781186548,-8.65956056235493E-17));
#5552=DIRECTION('center_axis',(0.,-1.,0.));
#5553=DIRECTION('ref_axis',(0.,0.,-1.));
#5554=DIRECTION('center_axis',(0.866025403784439,0.,-0.5));
#5555=DIRECTION('ref_axis',(0.5,0.,0.866025403784439));
#5556=DIRECTION('',(-0.5,0.,-0.866025403784439));
#5557=DIRECTION('',(0.,-1.,0.));
#5558=DIRECTION('',(0.5,0.,0.866025403784439));
#5559=DIRECTION('',(0.,-1.,0.));
#5560=DIRECTION('center_axis',(1.60246890531964E-16,0.,-1.));
#5561=DIRECTION('ref_axis',(1.,0.,1.60246890531964E-16));
#5562=DIRECTION('',(-1.,0.,-1.60246890531964E-16));
#5563=DIRECTION('',(0.,-1.,0.));
#5564=DIRECTION('',(1.,0.,1.60246890531964E-16));
#5565=DIRECTION('center_axis',(-0.866025403784439,0.,-0.5));
#5566=DIRECTION('ref_axis',(0.5,0.,-0.866025403784439));
#5567=DIRECTION('',(-0.5,0.,0.866025403784439));
#5568=DIRECTION('',(0.,-1.,0.));
#5569=DIRECTION('',(0.5,0.,-0.866025403784439));
#5570=DIRECTION('center_axis',(-0.866025403784439,0.,0.5));
#5571=DIRECTION('ref_axis',(-0.5,0.,-0.866025403784439));
#5572=DIRECTION('',(0.5,0.,0.866025403784439));
#5573=DIRECTION('',(0.,-1.,0.));
#5574=DIRECTION('',(-0.5,0.,-0.866025403784439));
#5575=DIRECTION('center_axis',(-1.60246890531964E-16,0.,1.));
#5576=DIRECTION('ref_axis',(-1.,0.,-1.60246890531964E-16));
#5577=DIRECTION('',(1.,0.,1.60246890531964E-16));
#5578=DIRECTION('',(0.,-1.,0.));
#5579=DIRECTION('',(-1.,0.,-1.60246890531964E-16));
#5580=DIRECTION('center_axis',(0.866025403784439,0.,0.5));
#5581=DIRECTION('ref_axis',(-0.5,0.,0.866025403784439));
#5582=DIRECTION('',(0.5,0.,-0.866025403784439));
#5583=DIRECTION('',(-0.5,0.,0.866025403784439));
#5584=DIRECTION('center_axis',(0.,1.,0.));
#5585=DIRECTION('ref_axis',(1.,0.,0.));
#5586=DIRECTION('center_axis',(0.,-1.,0.));
#5587=DIRECTION('ref_axis',(0.,0.,-1.));
#6635=CARTESIAN_POINT('',(0.,0.,0.));
#6636=CARTESIAN_POINT('Origin',(0.6,0.8,0.));
#6637=CARTESIAN_POINT('',(-0.6,0.8,-7.34788079488412E-17));
#6638=CARTESIAN_POINT('Origin',(0.,0.8,0.));
#6639=CARTESIAN_POINT('Origin',(0.,0.775,0.));
#6640=CARTESIAN_POINT('',(-0.65,0.75,-7.9602041944578E-17));
#6641=CARTESIAN_POINT('Origin',(0.,0.75,0.));
#6642=CARTESIAN_POINT('',(-0.625,0.775,-7.65404249467096E-17));
#6643=CARTESIAN_POINT('Origin',(0.,0.39,0.));
#6644=CARTESIAN_POINT('',(-0.65,0.0299999999999998,-7.9602041944578E-17));
#6645=CARTESIAN_POINT('Origin',(0.,0.0299999999999998,0.));
#6646=CARTESIAN_POINT('',(-0.65,0.39,-7.9602041944578E-17));
#6647=CARTESIAN_POINT('Origin',(0.,0.0150000000000001,0.));
#6648=CARTESIAN_POINT('',(-0.62,5.89805981832114E-17,-7.59281015471359E-17));
#6649=CARTESIAN_POINT('Origin',(0.,0.,0.));
#6650=CARTESIAN_POINT('',(-0.635,0.0150000000000001,-7.77650717458569E-17));
#6651=CARTESIAN_POINT('Origin',(0.42,0.,0.));
#6652=CARTESIAN_POINT('',(-0.42,-3.46944695195361E-18,-5.14351655641888E-17));
#6653=CARTESIAN_POINT('Origin',(0.,0.,0.));
#6654=CARTESIAN_POINT('Origin',(0.,-0.02,0.));
#6655=CARTESIAN_POINT('',(-0.3933,-0.0534000000000001,4.81653586104654E-17));
#6656=CARTESIAN_POINT('Origin',(0.,-0.0534000000000001,0.));
#6657=CARTESIAN_POINT('',(-0.41,-0.02,-5.02105187650415E-17));
#6658=CARTESIAN_POINT('Origin',(0.,-1.48,0.));
#6659=CARTESIAN_POINT('',(-0.3933,-2.9267,4.81653586104654E-17));
#6660=CARTESIAN_POINT('Origin',(0.,-2.9267,0.));
#6661=CARTESIAN_POINT('',(-0.3933,-1.48,-4.81653586104654E-17));
#6662=CARTESIAN_POINT('Origin',(0.,-2.96,0.));
#6663=CARTESIAN_POINT('',(-0.32,-3.,-3.91886975727153E-17));
#6664=CARTESIAN_POINT('Origin',(0.,-3.,0.));
#6665=CARTESIAN_POINT('',(-0.36,-2.96,-4.40872847693047E-17));
#6666=CARTESIAN_POINT('Origin',(0.,-3.,0.));
#6667=CARTESIAN_POINT('Origin',(0.173205080756888,-0.8,-0.3));
#6668=CARTESIAN_POINT('',(0.346410161513775,-0.8,0.));
#6669=CARTESIAN_POINT('',(0.173205080756888,-0.8,-0.3));
#6670=CARTESIAN_POINT('',(0.346410161513775,-0.8,0.));
#6671=CARTESIAN_POINT('',(0.173205080756888,-1.28,-0.3));
#6672=CARTESIAN_POINT('',(0.173205080756888,-0.8,-0.3));
#6673=CARTESIAN_POINT('',(0.346410161513775,-1.28,0.));
#6674=CARTESIAN_POINT('',(0.346410161513775,-1.28,0.));
#6675=CARTESIAN_POINT('',(0.346410161513775,-0.8,0.));
#6676=CARTESIAN_POINT('Origin',(-0.173205080756888,-0.8,-0.3));
#6677=CARTESIAN_POINT('',(-0.173205080756888,-0.8,-0.3));
#6678=CARTESIAN_POINT('',(0.173205080756888,-0.8,-0.3));
#6679=CARTESIAN_POINT('',(-0.173205080756888,-1.28,-0.3));
#6680=CARTESIAN_POINT('',(-0.173205080756888,-0.8,-0.3));
#6681=CARTESIAN_POINT('',(0.173205080756888,-1.28,-0.3));
#6682=CARTESIAN_POINT('Origin',(-0.346410161513775,-0.8,-5.55111512312578E-17));
#6683=CARTESIAN_POINT('',(-0.346410161513775,-0.8,-4.24230095489963E-17));
#6684=CARTESIAN_POINT('',(-0.173205080756888,-0.8,-0.3));
#6685=CARTESIAN_POINT('',(-0.346410161513775,-1.28,-5.55111512312578E-17));
#6686=CARTESIAN_POINT('',(-0.346410161513775,-0.8,-4.24230095489963E-17));
#6687=CARTESIAN_POINT('',(-0.173205080756888,-1.28,-0.3));
#6688=CARTESIAN_POINT('Origin',(-0.173205080756888,-0.8,0.3));
#6689=CARTESIAN_POINT('',(-0.173205080756888,-0.8,0.3));
#6690=CARTESIAN_POINT('',(-0.346410161513775,-0.8,-4.24230095489963E-17));
#6691=CARTESIAN_POINT('',(-0.173205080756888,-1.28,0.3));
#6692=CARTESIAN_POINT('',(-0.173205080756888,-0.8,0.3));
#6693=CARTESIAN_POINT('',(-0.346410161513775,-1.28,-4.24230095489963E-17));
#6694=CARTESIAN_POINT('Origin',(0.173205080756888,-0.8,0.3));
#6695=CARTESIAN_POINT('',(0.173205080756888,-0.8,0.3));
#6696=CARTESIAN_POINT('',(-0.173205080756888,-0.8,0.3));
#6697=CARTESIAN_POINT('',(0.173205080756888,-1.28,0.3));
#6698=CARTESIAN_POINT('',(0.173205080756888,-0.8,0.3));
#6699=CARTESIAN_POINT('',(-0.173205080756888,-1.28,0.3));
#6700=CARTESIAN_POINT('Origin',(0.346410161513775,-0.8,0.));
#6701=CARTESIAN_POINT('',(0.173205080756888,-0.8,0.3));
#6702=CARTESIAN_POINT('',(0.173205080756888,-1.28,0.3));
#6703=CARTESIAN_POINT('Origin',(0.,-0.8,-5.55111512312578E-17));
#6704=CARTESIAN_POINT('Origin',(0.,-1.28,-5.55111512312578E-17));
#6854=UNCERTAINTY_MEASURE_WITH_UNIT(LENGTH_MEASURE(0.001),#6879,
'DISTANCE_ACCURACY_VALUE',
'Maximum model space distance between geometric entities at asserted c
onnectivities');
#6857=UNCERTAINTY_MEASURE_WITH_UNIT(LENGTH_MEASURE(0.001),#6879,
'DISTANCE_ACCURACY_VALUE',
'Maximum model space distance between geometric entities at asserted c
onnectivities');
#6875=(
GEOMETRIC_REPRESENTATION_CONTEXT(3)
GLOBAL_UNCERTAINTY_ASSIGNED_CONTEXT((#6854))
GLOBAL_UNIT_ASSIGNED_CONTEXT((#6879,#6881,#6882))
REPRESENTATION_CONTEXT('','3D')
);
#6878=(
GEOMETRIC_REPRESENTATION_CONTEXT(3)
GLOBAL_UNCERTAINTY_ASSIGNED_CONTEXT((#6857))
GLOBAL_UNIT_ASSIGNED_CONTEXT((#6879,#6881,#6882))
REPRESENTATION_CONTEXT('','3D')
);
#6879=(
LENGTH_UNIT()
NAMED_UNIT(*)
SI_UNIT(.CENTI.,.METRE.)
);
#6881=(
NAMED_UNIT(*)
PLANE_ANGLE_UNIT()
SI_UNIT($,.RADIAN.)
);
#6882=(
NAMED_UNIT(*)
SI_UNIT($,.STERADIAN.)
SOLID_ANGLE_UNIT()
);
#6900=SHAPE_DEFINITION_REPRESENTATION(#6920,#6980);
#6920=PRODUCT_DEFINITION_SHAPE('',$,#7001);
#6980=SHAPE_REPRESENTATION('',(#4443),#6875);
#6983=PRODUCT_DEFINITION_CONTEXT('part definition',#7045,'design');
#7001=PRODUCT_DEFINITION('Cap Screw - M8x30',
'Cap Screw - M8x30',#7021,#6983);
#7021=PRODUCT_DEFINITION_FORMATION('',$,#7064);
#7045=APPLICATION_CONTEXT(
'Core Data for Automotive Mechanical Design Process');
#7046=PRODUCT_CONTEXT('part definition',#7045,'mechanical');
#7064=PRODUCT('Cap Screw - M8x30','Cap Screw - M8x30',
'Cap Screw - M8x30',(#7046));
#7130=COLOUR_RGB('Black',0.12,0.14,0.17);
#7131=FILL_AREA_STYLE_COLOUR('',#7130);
#7132=FILL_AREA_STYLE('',(#7131));
#7133=SURFACE_STYLE_FILL_AREA(#7132);
#7134=SURFACE_SIDE_STYLE('',(#7133));
#7135=SURFACE_STYLE_USAGE(.BOTH.,#7134);
#7136=PRESENTATION_STYLE_ASSIGNMENT((#7135));
ENDSEC;
END-ISO-10303-21;
